ISO-10303-21;
HEADER;
/* Generated by software containing ST-Developer
 * from STEP Tools, Inc. (www.steptools.com) 
 */
/* OPTION: using custom renumber hook */

FILE_DESCRIPTION(
/* description */ ('STEP AP242 Edition 2', 'CAx-IF Rec.Pracs.---Representation and Presentation of Product Manufa
cturing Information (PMI)---4.0---2014-10-13', 'CAx-IF Rec.Pracs.---3D Tessellated Geometry---0.4---2014-09-14', '2;1', 'CAx-IF Rec.Pracs.---User Defined Attributes---1.5---2016-08-15'),
/* implementation_level */ '2;1');

FILE_NAME(
/* name */ 'o_ring.step',
/* time_stamp */ '2026-10-08T12:15:07Z',
/* author */ (''),
/* organization */ (''),
/* preprocessor_version */ 'ST-DEVELOPER v20',
/* originating_system */ 'ONSHAPE BY PTC INC, 1.221',
/* authorisation */ '  ');

FILE_SCHEMA (('AP242_MANAGED_MODEL_BASED_3D_ENGINEERING_MIM_LF { 1 0 10303 442 3 1 4 }'));
ENDSEC;

DATA;
#64=COLOUR_RGB('', 0.31764706, 0.68627451, 0.89019608);
#227=SHAPE_REPRESENTATION_RELATIONSHIP('','',#13801,#254);
#254=ADVANCED_BREP_SHAPE_REPRESENTATION('',(#13745),#45491);
#336=TOROIDAL_SURFACE('',#15293,0.0093,0.001);
#1060=CIRCLE('',#15291,0.01);
#1061=CIRCLE('',#15292,0.01);
#1825=CYLINDRICAL_SURFACE('',#15290,0.01);
#5626=ORIENTED_EDGE('',*,*,#7460,.F.);
#5627=ORIENTED_EDGE('',*,*,#7461,.T.);
#5628=ORIENTED_EDGE('',*,*,#7461,.F.);
#5629=ORIENTED_EDGE('',*,*,#7460,.T.);
#7460=EDGE_CURVE('',#8771,#8771,#1060,.T.);
#7461=EDGE_CURVE('',#8772,#8772,#1061,.T.);
#8771=VERTEX_POINT('',#45458);
#8772=VERTEX_POINT('',#45460);
#11540=EDGE_LOOP('',(#5626));
#11541=EDGE_LOOP('',(#5627));
#11542=EDGE_LOOP('',(#5628));
#11543=EDGE_LOOP('',(#5629));
#12659=FACE_BOUND('',#11540,.T.);
#12660=FACE_BOUND('',#11541,.T.);
#12661=FACE_BOUND('',#11542,.T.);
#12662=FACE_BOUND('',#11543,.T.);
#13500=ADVANCED_FACE('',(#12659,#12660),#1825,.T.);
#13501=ADVANCED_FACE('',(#12661,#12662),#336,.T.);
#13528=CLOSED_SHELL('',(#13500,#13501));
#13555=STYLED_ITEM('',(#13582),#13745);
#13582=PRESENTATION_STYLE_ASSIGNMENT((#13609));
#13609=SURFACE_STYLE_USAGE(.BOTH.,#13636);
#13636=SURFACE_SIDE_STYLE('',(#13663));
#13663=SURFACE_STYLE_FILL_AREA(#13690);
#13690=FILL_AREA_STYLE('',(#13717));
#13717=FILL_AREA_STYLE_COLOUR('',#64);
#13745=MANIFOLD_SOLID_BREP('o_ring',#13528);
#13773=SHAPE_DEFINITION_REPRESENTATION(#45583,#13801);
#13801=SHAPE_REPRESENTATION('o_ring',(#13802),#45491);
#13802=AXIS2_PLACEMENT_3D('',#19109,#15295,#15296);
#15290=AXIS2_PLACEMENT_3D('',#45456,#19099,#19100);
#15291=AXIS2_PLACEMENT_3D('',#45457,#19101,#19102);
#15292=AXIS2_PLACEMENT_3D('',#45459,#19103,#19104);
#15293=AXIS2_PLACEMENT_3D('',#45461,#19105,#19106);
#15295=DIRECTION('',(0.,0.,1.));
#15296=DIRECTION('',(1.,0.,0.));
#19099=DIRECTION('',(0.,0.,-1.));
#19100=DIRECTION('',(-1.,0.,0.));
#19101=DIRECTION('',(0.,0.,-1.));
#19102=DIRECTION('',(-1.,0.,0.));
#19103=DIRECTION('',(0.,0.,-1.));
#19104=DIRECTION('',(-1.,0.,0.));
#19105=DIRECTION('',(0.,0.,-1.));
#19106=DIRECTION('',(-1.,0.,0.));
#19109=CARTESIAN_POINT('',(0.,0.,0.));
#45456=CARTESIAN_POINT('',(0.,0.,-0.0300923697749146));
#45457=CARTESIAN_POINT('',(0.,0.,0.00891153628714572));
#45458=CARTESIAN_POINT('',(-0.01,0.,0.00891153628714572));
#45459=CARTESIAN_POINT('',(0.,0.,0.0103398219728543));
#45460=CARTESIAN_POINT('',(-0.01,0.,0.0103398219728543));
#45461=CARTESIAN_POINT('',(0.,0.,0.00962567913));
#45463=MECHANICAL_DESIGN_GEOMETRIC_PRESENTATION_REPRESENTATION('',(#13555),#45464);
#45464=(
GEOMETRIC_REPRESENTATION_CONTEXT(3)
GLOBAL_UNCERTAINTY_ASSIGNED_CONTEXT((#45492))
GLOBAL_UNIT_ASSIGNED_CONTEXT((#45522,#45521,#45520))
REPRESENTATION_CONTEXT('MAS-690','TOP_LEVEL_ASSEMBLY_PART')
);
#45491=(
GEOMETRIC_REPRESENTATION_CONTEXT(3)
GLOBAL_UNCERTAINTY_ASSIGNED_CONTEXT((#45519))
GLOBAL_UNIT_ASSIGNED_CONTEXT((#45522,#45521,#45520))
REPRESENTATION_CONTEXT('o_ring','COMPONENT_PART')
);
#45492=UNCERTAINTY_MEASURE_WITH_UNIT(LENGTH_MEASURE(1.E-8),#45522,
'DISTANCE_ACCURACY_VALUE','Maximum Tolerance applied to model');
#45519=UNCERTAINTY_MEASURE_WITH_UNIT(LENGTH_MEASURE(1.E-8),#45522,
'DISTANCE_ACCURACY_VALUE','Maximum Tolerance applied to model');
#45520=(
NAMED_UNIT(*)
SI_UNIT($,.STERADIAN.)
SOLID_ANGLE_UNIT()
);
#45521=(
NAMED_UNIT(*)
PLANE_ANGLE_UNIT()
SI_UNIT($,.RADIAN.)
);
#45522=(
LENGTH_UNIT()
NAMED_UNIT(*)
SI_UNIT($,.METRE.)
);
#45583=PRODUCT_DEFINITION_SHAPE('','',#45612);
#45612=PRODUCT_DEFINITION('','',#45668,#45640);
#45640=PRODUCT_DEFINITION_CONTEXT('',#45782,'design');
#45668=PRODUCT_DEFINITION_FORMATION_WITH_SPECIFIED_SOURCE('','',#45724,
 .NOT_KNOWN.);
#45724=PRODUCT('o_ring','o_ring','o_ring',(#45780));
#45780=PRODUCT_CONTEXT('',#45782,'mechanical');
#45782=APPLICATION_CONTEXT('managed model based 3d engineering');
ENDSEC;
END-ISO-10303-21;
